ISO-10303-21;
HEADER;
/* Generated by software containing ST-Developer
 * from STEP Tools, Inc. (www.steptools.com) 
 */

FILE_DESCRIPTION(
/* description */ ('XY cross-slide table'),
/* implementation_level */ '2;1');

FILE_NAME(
/* name */ 'Socket Set Screw - M5x8 (1).step',
/* time_stamp */ '2026-10-28T03:22:46-07:00',
/* author */ (''),
/* organization */ (''),
/* preprocessor_version */ 'ST-DEVELOPER v20.2',
/* originating_system */ 'Autodesk Translation Framework v15.17.0.0',
/* authorisation */ '');

FILE_SCHEMA (('AUTOMOTIVE_DESIGN { 1 0 10303 214 3 1 1 }'));
ENDSEC;

DATA;
#10=MECHANICAL_DESIGN_GEOMETRIC_PRESENTATION_REPRESENTATION('',(#1780),#62984);
#1490=CONICAL_SURFACE('',#26368,0.235,0.785398163397448);
#1491=CONICAL_SURFACE('',#26372,0.2125,0.785398163397448);
#1584=SHAPE_REPRESENTATION_RELATIONSHIP('SRR','None',#63444,#1667);
#1667=ADVANCED_BREP_SHAPE_REPRESENTATION('',(#1885),#62981);
#1780=STYLED_ITEM('',(#63919),#1885);
#1885=MANIFOLD_SOLID_BREP('Body1',#23082);
#2292=FACE_BOUND('',#5877,.T.);
#2847=PLANE('',#26359);
#2848=PLANE('',#26360);
#2849=PLANE('',#26361);
#2850=PLANE('',#26362);
#2851=PLANE('',#26363);
#2852=PLANE('',#26364);
#2853=PLANE('',#26365);
#2854=PLANE('',#26366);
#2855=PLANE('',#26374);
#4150=FACE_OUTER_BOUND('',#5869,.T.);
#4151=FACE_OUTER_BOUND('',#5870,.T.);
#4152=FACE_OUTER_BOUND('',#5871,.T.);
#4153=FACE_OUTER_BOUND('',#5872,.T.);
#4154=FACE_OUTER_BOUND('',#5873,.T.);
#4155=FACE_OUTER_BOUND('',#5874,.T.);
#4156=FACE_OUTER_BOUND('',#5875,.T.);
#4157=FACE_OUTER_BOUND('',#5876,.T.);
#4158=FACE_OUTER_BOUND('',#5878,.T.);
#4159=FACE_OUTER_BOUND('',#5879,.T.);
#4160=FACE_OUTER_BOUND('',#5880,.T.);
#4161=FACE_OUTER_BOUND('',#5881,.T.);
#5869=EDGE_LOOP('',(#20914,#20915,#20916,#20917));
#5870=EDGE_LOOP('',(#20918,#20919,#20920,#20921));
#5871=EDGE_LOOP('',(#20922,#20923,#20924,#20925));
#5872=EDGE_LOOP('',(#20926,#20927,#20928,#20929));
#5873=EDGE_LOOP('',(#20930,#20931,#20932,#20933));
#5874=EDGE_LOOP('',(#20934,#20935,#20936,#20937));
#5875=EDGE_LOOP('',(#20938,#20939,#20940,#20941,#20942,#20943));
#5876=EDGE_LOOP('',(#20944));
#5877=EDGE_LOOP('',(#20945,#20946,#20947,#20948,#20949,#20950));
#5878=EDGE_LOOP('',(#20951,#20952,#20953,#20954));
#5879=EDGE_LOOP('',(#20955,#20956,#20957,#20958));
#5880=EDGE_LOOP('',(#20959,#20960,#20961,#20962));
#5881=EDGE_LOOP('',(#20963));
#7346=LINE('',#62601,#8833);
#7347=LINE('',#62603,#8834);
#7348=LINE('',#62605,#8835);
#7349=LINE('',#62606,#8836);
#7350=LINE('',#62609,#8837);
#7351=LINE('',#62611,#8838);
#7352=LINE('',#62612,#8839);
#7353=LINE('',#62615,#8840);
#7354=LINE('',#62617,#8841);
#7355=LINE('',#62618,#8842);
#7356=LINE('',#62621,#8843);
#7357=LINE('',#62623,#8844);
#7358=LINE('',#62624,#8845);
#7359=LINE('',#62627,#8846);
#7360=LINE('',#62629,#8847);
#7361=LINE('',#62630,#8848);
#7362=LINE('',#62632,#8849);
#7363=LINE('',#62633,#8850);
#7364=LINE('',#62641,#8851);
#7365=LINE('',#62645,#8852);
#7366=LINE('',#62649,#8853);
#8833=VECTOR('',#32621,1.);
#8834=VECTOR('',#32622,1.);
#8835=VECTOR('',#32623,1.);
#8836=VECTOR('',#32624,1.);
#8837=VECTOR('',#32627,1.);
#8838=VECTOR('',#32628,1.);
#8839=VECTOR('',#32629,1.);
#8840=VECTOR('',#32632,1.);
#8841=VECTOR('',#32633,1.);
#8842=VECTOR('',#32634,1.);
#8843=VECTOR('',#32637,1.);
#8844=VECTOR('',#32638,1.);
#8845=VECTOR('',#32639,1.);
#8846=VECTOR('',#32642,1.);
#8847=VECTOR('',#32643,1.);
#8848=VECTOR('',#32644,1.);
#8849=VECTOR('',#32647,1.);
#8850=VECTOR('',#32648,1.);
#8851=VECTOR('',#32659,0.235);
#8852=VECTOR('',#32664,0.25);
#8853=VECTOR('',#32669,0.2125);
#9757=CIRCLE('',#26367,0.22);
#9758=CIRCLE('',#26369,0.24505);
#9759=CIRCLE('',#26371,0.24505);
#9760=CIRCLE('',#26373,0.175);
#11796=VERTEX_POINT('',#62599);
#11797=VERTEX_POINT('',#62600);
#11798=VERTEX_POINT('',#62602);
#11799=VERTEX_POINT('',#62604);
#11800=VERTEX_POINT('',#62608);
#11801=VERTEX_POINT('',#62610);
#11802=VERTEX_POINT('',#62614);
#11803=VERTEX_POINT('',#62616);
#11804=VERTEX_POINT('',#62620);
#11805=VERTEX_POINT('',#62622);
#11806=VERTEX_POINT('',#62626);
#11807=VERTEX_POINT('',#62628);
#11808=VERTEX_POINT('',#62636);
#11809=VERTEX_POINT('',#62639);
#11810=VERTEX_POINT('',#62643);
#11811=VERTEX_POINT('',#62647);
#14841=EDGE_CURVE('',#11796,#11797,#7346,.T.);
#14842=EDGE_CURVE('',#11796,#11798,#7347,.T.);
#14843=EDGE_CURVE('',#11798,#11799,#7348,.T.);
#14844=EDGE_CURVE('',#11797,#11799,#7349,.T.);
#14845=EDGE_CURVE('',#11800,#11796,#7350,.T.);
#14846=EDGE_CURVE('',#11800,#11801,#7351,.T.);
#14847=EDGE_CURVE('',#11801,#11798,#7352,.T.);
#14848=EDGE_CURVE('',#11802,#11800,#7353,.T.);
#14849=EDGE_CURVE('',#11802,#11803,#7354,.T.);
#14850=EDGE_CURVE('',#11803,#11801,#7355,.T.);
#14851=EDGE_CURVE('',#11804,#11802,#7356,.T.);
#14852=EDGE_CURVE('',#11804,#11805,#7357,.T.);
#14853=EDGE_CURVE('',#11805,#11803,#7358,.T.);
#14854=EDGE_CURVE('',#11806,#11804,#7359,.T.);
#14855=EDGE_CURVE('',#11806,#11807,#7360,.T.);
#14856=EDGE_CURVE('',#11807,#11805,#7361,.T.);
#14857=EDGE_CURVE('',#11797,#11806,#7362,.T.);
#14858=EDGE_CURVE('',#11799,#11807,#7363,.T.);
#14859=EDGE_CURVE('',#11808,#11808,#9757,.T.);
#14860=EDGE_CURVE('',#11809,#11809,#9758,.T.);
#14861=EDGE_CURVE('',#11809,#11808,#7364,.T.);
#14862=EDGE_CURVE('',#11810,#11810,#9759,.F.);
#14863=EDGE_CURVE('',#11810,#11809,#7365,.T.);
#14864=EDGE_CURVE('',#11811,#11811,#9760,.T.);
#14865=EDGE_CURVE('',#11811,#11810,#7366,.T.);
#20914=ORIENTED_EDGE('',*,*,#14841,.F.);
#20915=ORIENTED_EDGE('',*,*,#14842,.T.);
#20916=ORIENTED_EDGE('',*,*,#14843,.T.);
#20917=ORIENTED_EDGE('',*,*,#14844,.F.);
#20918=ORIENTED_EDGE('',*,*,#14845,.F.);
#20919=ORIENTED_EDGE('',*,*,#14846,.T.);
#20920=ORIENTED_EDGE('',*,*,#14847,.T.);
#20921=ORIENTED_EDGE('',*,*,#14842,.F.);
#20922=ORIENTED_EDGE('',*,*,#14848,.F.);
#20923=ORIENTED_EDGE('',*,*,#14849,.T.);
#20924=ORIENTED_EDGE('',*,*,#14850,.T.);
#20925=ORIENTED_EDGE('',*,*,#14846,.F.);
#20926=ORIENTED_EDGE('',*,*,#14851,.F.);
#20927=ORIENTED_EDGE('',*,*,#14852,.T.);
#20928=ORIENTED_EDGE('',*,*,#14853,.T.);
#20929=ORIENTED_EDGE('',*,*,#14849,.F.);
#20930=ORIENTED_EDGE('',*,*,#14854,.F.);
#20931=ORIENTED_EDGE('',*,*,#14855,.T.);
#20932=ORIENTED_EDGE('',*,*,#14856,.T.);
#20933=ORIENTED_EDGE('',*,*,#14852,.F.);
#20934=ORIENTED_EDGE('',*,*,#14857,.F.);
#20935=ORIENTED_EDGE('',*,*,#14844,.T.);
#20936=ORIENTED_EDGE('',*,*,#14858,.T.);
#20937=ORIENTED_EDGE('',*,*,#14855,.F.);
#20938=ORIENTED_EDGE('',*,*,#14858,.F.);
#20939=ORIENTED_EDGE('',*,*,#14843,.F.);
#20940=ORIENTED_EDGE('',*,*,#14847,.F.);
#20941=ORIENTED_EDGE('',*,*,#14850,.F.);
#20942=ORIENTED_EDGE('',*,*,#14853,.F.);
#20943=ORIENTED_EDGE('',*,*,#14856,.F.);
#20944=ORIENTED_EDGE('',*,*,#14859,.F.);
#20945=ORIENTED_EDGE('',*,*,#14841,.T.);
#20946=ORIENTED_EDGE('',*,*,#14857,.T.);
#20947=ORIENTED_EDGE('',*,*,#14854,.T.);
#20948=ORIENTED_EDGE('',*,*,#14851,.T.);
#20949=ORIENTED_EDGE('',*,*,#14848,.T.);
#20950=ORIENTED_EDGE('',*,*,#14845,.T.);
#20951=ORIENTED_EDGE('',*,*,#14860,.F.);
#20952=ORIENTED_EDGE('',*,*,#14861,.T.);
#20953=ORIENTED_EDGE('',*,*,#14859,.T.);
#20954=ORIENTED_EDGE('',*,*,#14861,.F.);
#20955=ORIENTED_EDGE('',*,*,#14862,.F.);
#20956=ORIENTED_EDGE('',*,*,#14863,.T.);
#20957=ORIENTED_EDGE('',*,*,#14860,.T.);
#20958=ORIENTED_EDGE('',*,*,#14863,.F.);
#20959=ORIENTED_EDGE('',*,*,#14864,.F.);
#20960=ORIENTED_EDGE('',*,*,#14865,.T.);
#20961=ORIENTED_EDGE('',*,*,#14862,.T.);
#20962=ORIENTED_EDGE('',*,*,#14865,.F.);
#20963=ORIENTED_EDGE('',*,*,#14864,.T.);
#21645=CYLINDRICAL_SURFACE('',#26370,0.24505);
#22931=ADVANCED_FACE('',(#4150),#2847,.F.);
#22932=ADVANCED_FACE('',(#4151),#2848,.F.);
#22933=ADVANCED_FACE('',(#4152),#2849,.F.);
#22934=ADVANCED_FACE('',(#4153),#2850,.F.);
#22935=ADVANCED_FACE('',(#4154),#2851,.F.);
#22936=ADVANCED_FACE('',(#4155),#2852,.F.);
#22937=ADVANCED_FACE('',(#4156),#2853,.F.);
#22938=ADVANCED_FACE('',(#4157,#2292),#2854,.T.);
#22939=ADVANCED_FACE('',(#4158),#1490,.T.);
#22940=ADVANCED_FACE('',(#4159),#21645,.T.);
#22941=ADVANCED_FACE('',(#4160),#1491,.T.);
#22942=ADVANCED_FACE('',(#4161),#2855,.T.);
#23082=CLOSED_SHELL('',(#22931,#22932,#22933,#22934,#22935,#22936,#22937,
#22938,#22939,#22940,#22941,#22942));
#26358=AXIS2_PLACEMENT_3D('',#62597,#32617,#32618);
#26359=AXIS2_PLACEMENT_3D('',#62598,#32619,#32620);
#26360=AXIS2_PLACEMENT_3D('',#62607,#32625,#32626);
#26361=AXIS2_PLACEMENT_3D('',#62613,#32630,#32631);
#26362=AXIS2_PLACEMENT_3D('',#62619,#32635,#32636);
#26363=AXIS2_PLACEMENT_3D('',#62625,#32640,#32641);
#26364=AXIS2_PLACEMENT_3D('',#62631,#32645,#32646);
#26365=AXIS2_PLACEMENT_3D('',#62634,#32649,#32650);
#26366=AXIS2_PLACEMENT_3D('',#62635,#32651,#32652);
#26367=AXIS2_PLACEMENT_3D('',#62637,#32653,#32654);
#26368=AXIS2_PLACEMENT_3D('',#62638,#32655,#32656);
#26369=AXIS2_PLACEMENT_3D('',#62640,#32657,#32658);
#26370=AXIS2_PLACEMENT_3D('',#62642,#32660,#32661);
#26371=AXIS2_PLACEMENT_3D('',#62644,#32662,#32663);
#26372=AXIS2_PLACEMENT_3D('',#62646,#32665,#32666);
#26373=AXIS2_PLACEMENT_3D('',#62648,#32667,#32668);
#26374=AXIS2_PLACEMENT_3D('',#62650,#32670,#32671);
#32617=DIRECTION('axis',(0.,0.,1.));
#32618=DIRECTION('refdir',(1.,0.,0.));
#32619=DIRECTION('center_axis',(0.866025403784439,0.,-0.5));
#32620=DIRECTION('ref_axis',(0.5,0.,0.866025403784439));
#32621=DIRECTION('',(0.5,0.,0.866025403784439));
#32622=DIRECTION('',(0.,-1.,0.));
#32623=DIRECTION('',(0.5,0.,0.866025403784439));
#32624=DIRECTION('',(0.,-1.,0.));
#32625=DIRECTION('center_axis',(1.92296268638356E-16,0.,-1.));
#32626=DIRECTION('ref_axis',(1.,0.,1.92296268638356E-16));
#32627=DIRECTION('',(1.,0.,1.92296268638356E-16));
#32628=DIRECTION('',(0.,-1.,0.));
#32629=DIRECTION('',(1.,0.,1.92296268638356E-16));
#32630=DIRECTION('center_axis',(-0.866025403784439,0.,-0.5));
#32631=DIRECTION('ref_axis',(0.5,0.,-0.866025403784439));
#32632=DIRECTION('',(0.5,0.,-0.866025403784439));
#32633=DIRECTION('',(0.,-1.,0.));
#32634=DIRECTION('',(0.5,0.,-0.866025403784438));
#32635=DIRECTION('center_axis',(-0.866025403784439,0.,0.5));
#32636=DIRECTION('ref_axis',(-0.5,0.,-0.866025403784439));
#32637=DIRECTION('',(-0.5,0.,-0.866025403784439));
#32638=DIRECTION('',(0.,-1.,0.));
#32639=DIRECTION('',(-0.5,0.,-0.866025403784439));
#32640=DIRECTION('center_axis',(-1.92296268638356E-16,0.,1.));
#32641=DIRECTION('ref_axis',(-1.,0.,-1.92296268638356E-16));
#32642=DIRECTION('',(-1.,0.,-1.92296268638356E-16));
#32643=DIRECTION('',(0.,-1.,0.));
#32644=DIRECTION('',(-1.,0.,-1.92296268638356E-16));
#32645=DIRECTION('center_axis',(0.866025403784439,0.,0.5));
#32646=DIRECTION('ref_axis',(-0.5,0.,0.866025403784439));
#32647=DIRECTION('',(-0.5,0.,0.866025403784439));
#32648=DIRECTION('',(-0.5,0.,0.866025403784439));
#32649=DIRECTION('center_axis',(0.,-1.,0.));
#32650=DIRECTION('ref_axis',(0.,0.,-1.));
#32651=DIRECTION('center_axis',(0.,1.,0.));
#32652=DIRECTION('ref_axis',(0.,0.,1.));
#32653=DIRECTION('center_axis',(0.,-1.,0.));
#32654=DIRECTION('ref_axis',(1.,0.,0.));
#32655=DIRECTION('center_axis',(0.,-1.,0.));
#32656=DIRECTION('ref_axis',(1.,0.,0.));
#32657=DIRECTION('center_axis',(0.,-1.,0.));
#32658=DIRECTION('ref_axis',(1.,0.,0.));
#32659=DIRECTION('',(0.707106781186547,0.707106781186548,8.65956056235493E-17));
#32660=DIRECTION('center_axis',(0.,-1.,0.));
#32661=DIRECTION('ref_axis',(1.,0.,0.));
#32662=DIRECTION('center_axis',(0.,1.,0.));
#32663=DIRECTION('ref_axis',(1.,0.,0.));
#32664=DIRECTION('',(0.,1.,0.));
#32665=DIRECTION('center_axis',(0.,1.,0.));
#32666=DIRECTION('ref_axis',(1.,0.,0.));
#32667=DIRECTION('center_axis',(0.,-1.,0.));
#32668=DIRECTION('ref_axis',(1.,0.,0.));
#32669=DIRECTION('',(-0.707106781186547,0.707106781186548,-8.65956056235493E-17));
#32670=DIRECTION('center_axis',(0.,-1.,0.));
#32671=DIRECTION('ref_axis',(0.,0.,-1.));
#62597=CARTESIAN_POINT('',(0.,0.,0.));
#62598=CARTESIAN_POINT('Origin',(0.0721687836487032,0.,-0.125));
#62599=CARTESIAN_POINT('',(0.0721687836487032,0.,-0.125));
#62600=CARTESIAN_POINT('',(0.144337567297406,0.,0.));
#62601=CARTESIAN_POINT('',(0.117710979560879,0.,-0.0461186027918559));
#62602=CARTESIAN_POINT('',(0.0721687836487032,-0.25,-0.125));
#62603=CARTESIAN_POINT('',(0.0721687836487032,0.,-0.125));
#62604=CARTESIAN_POINT('',(0.144337567297406,-0.25,0.));
#62605=CARTESIAN_POINT('',(0.144337567297406,-0.25,0.));
#62606=CARTESIAN_POINT('',(0.144337567297406,0.,0.));
#62607=CARTESIAN_POINT('Origin',(-0.0721687836487032,0.,-0.125));
#62608=CARTESIAN_POINT('',(-0.0721687836487032,0.,-0.125));
#62609=CARTESIAN_POINT('',(0.0739156081756484,0.,-0.125));
#62610=CARTESIAN_POINT('',(-0.0721687836487032,-0.25,-0.125));
#62611=CARTESIAN_POINT('',(-0.0721687836487032,0.,-0.125));
#62612=CARTESIAN_POINT('',(0.0721687836487032,-0.25,-0.125));
#62613=CARTESIAN_POINT('Origin',(-0.144337567297406,0.,-4.16333634234434E-17));
#62614=CARTESIAN_POINT('',(-0.144337567297406,0.,-1.76762539787485E-17));
#62615=CARTESIAN_POINT('',(-0.0987953713852306,0.,-0.0788813972081442));
#62616=CARTESIAN_POINT('',(-0.144337567297406,-0.25,-2.77555756156289E-17));
#62617=CARTESIAN_POINT('',(-0.144337567297406,0.,-1.76762539787485E-17));
#62618=CARTESIAN_POINT('',(-0.0721687836487032,-0.25,-0.125));
#62619=CARTESIAN_POINT('Origin',(-0.0721687836487033,0.,0.125));
#62620=CARTESIAN_POINT('',(-0.0721687836487033,0.,0.125));
#62621=CARTESIAN_POINT('',(-0.0627109795608791,0.,0.141381397208144));
#62622=CARTESIAN_POINT('',(-0.0721687836487033,-0.25,0.125));
#62623=CARTESIAN_POINT('',(-0.0721687836487033,0.,0.125));
#62624=CARTESIAN_POINT('',(-0.144337567297406,-0.25,-1.76762539787485E-17));
#62625=CARTESIAN_POINT('Origin',(0.0721687836487032,0.,0.125));
#62626=CARTESIAN_POINT('',(0.0721687836487032,0.,0.125));
#62627=CARTESIAN_POINT('',(0.146084391824352,0.,0.125));
#62628=CARTESIAN_POINT('',(0.0721687836487032,-0.25,0.125));
#62629=CARTESIAN_POINT('',(0.0721687836487032,0.,0.125));
#62630=CARTESIAN_POINT('',(-0.0721687836487033,-0.25,0.125));
#62631=CARTESIAN_POINT('Origin',(0.144337567297406,0.,0.));
#62632=CARTESIAN_POINT('',(0.153795371385231,0.,-0.0163813972081441));
#62633=CARTESIAN_POINT('',(0.0721687836487032,-0.25,0.125));
#62634=CARTESIAN_POINT('Origin',(0.,-0.25,0.));
#62635=CARTESIAN_POINT('Origin',(0.22,0.,0.));
#62636=CARTESIAN_POINT('',(-0.22,-8.67361737988404E-18,-2.69422295812418E-17));
#62637=CARTESIAN_POINT('Origin',(0.,0.,0.));
#62638=CARTESIAN_POINT('Origin',(0.,-0.015,0.));
#62639=CARTESIAN_POINT('',(-0.24505,-0.02505,-3.00099698131059E-17));
#62640=CARTESIAN_POINT('Origin',(0.,-0.02505,0.));
#62641=CARTESIAN_POINT('',(-0.235,-0.015,-2.87791997799628E-17));
#62642=CARTESIAN_POINT('Origin',(0.,-0.3775,0.));
#62643=CARTESIAN_POINT('',(-0.24505,-0.72995,3.00099698131059E-17));
#62644=CARTESIAN_POINT('Origin',(0.,-0.72995,0.));
#62645=CARTESIAN_POINT('',(-0.24505,-0.3775,-3.00099698131059E-17));
#62646=CARTESIAN_POINT('Origin',(0.,-0.7625,0.));
#62647=CARTESIAN_POINT('',(-0.175,-0.8,-2.14313189850787E-17));
#62648=CARTESIAN_POINT('Origin',(0.,-0.8,0.));
#62649=CARTESIAN_POINT('',(-0.2125,-0.7625,-2.60237444818813E-17));
#62650=CARTESIAN_POINT('Origin',(0.,-0.8,0.));
#62882=UNCERTAINTY_MEASURE_WITH_UNIT(LENGTH_MEASURE(0.001),#62985,
'DISTANCE_ACCURACY_VALUE',
'Maximum model space distance between geometric entities at asserted c
onnectivities');
#62885=UNCERTAINTY_MEASURE_WITH_UNIT(LENGTH_MEASURE(0.001),#62985,
'DISTANCE_ACCURACY_VALUE',
'Maximum model space distance between geometric entities at asserted c
onnectivities');
#62981=(
GEOMETRIC_REPRESENTATION_CONTEXT(3)
GLOBAL_UNCERTAINTY_ASSIGNED_CONTEXT((#62882))
GLOBAL_UNIT_ASSIGNED_CONTEXT((#62985,#62987,#62988))
REPRESENTATION_CONTEXT('','3D')
);
#62984=(
GEOMETRIC_REPRESENTATION_CONTEXT(3)
GLOBAL_UNCERTAINTY_ASSIGNED_CONTEXT((#62885))
GLOBAL_UNIT_ASSIGNED_CONTEXT((#62985,#62987,#62988))
REPRESENTATION_CONTEXT('','3D')
);
#62985=(
LENGTH_UNIT()
NAMED_UNIT(*)
SI_UNIT(.CENTI.,.METRE.)
);
#62987=(
NAMED_UNIT(*)
PLANE_ANGLE_UNIT()
SI_UNIT($,.RADIAN.)
);
#62988=(
NAMED_UNIT(*)
SI_UNIT($,.STERADIAN.)
SOLID_ANGLE_UNIT()
);
#63084=SHAPE_DEFINITION_REPRESENTATION(#63295,#63444);
#63295=PRODUCT_DEFINITION_SHAPE('',$,#63543);
#63444=SHAPE_REPRESENTATION('',(#26358),#62981);
#63447=PRODUCT_DEFINITION_CONTEXT('part definition',#63743,'design');
#63543=PRODUCT_DEFINITION('Socket Set Screw - M5x8 (1)',
'Socket Set Screw - M5x8 (1)',#63641,#63447);
#63641=PRODUCT_DEFINITION_FORMATION('',$,#63840);
#63743=APPLICATION_CONTEXT(
'Core Data for Automotive Mechanical Design Process');
#63744=PRODUCT_CONTEXT('part definition',#63743,'mechanical');
#63840=PRODUCT('Socket Set Screw - M5x8 (1)',
'Socket Set Screw - M5x8 (1)','Socket Set Screw - M5x8 (1)',(#63744));
#63913=COLOUR_RGB('Black',0.12,0.14,0.17);
#63914=FILL_AREA_STYLE_COLOUR('',#63913);
#63915=FILL_AREA_STYLE('',(#63914));
#63916=SURFACE_STYLE_FILL_AREA(#63915);
#63917=SURFACE_SIDE_STYLE('',(#63916));
#63918=SURFACE_STYLE_USAGE(.BOTH.,#63917);
#63919=PRESENTATION_STYLE_ASSIGNMENT((#63918));
ENDSEC;
END-ISO-10303-21;
